ISO-10303-21;
HEADER;
FILE_DESCRIPTION (('STEP AP214'),
    '1' );
FILE_NAME ('socket head cap screw_iso_ISO 4762 M5 x 30 - 22N.step',
    '2026-10-31T03:46:07',
    ( '' ),
    ( '' ),
    'SwSTEP 2.0',
    'SolidWorks 2026',
    '' );
FILE_SCHEMA (( 'AUTOMOTIVE_DESIGN' ));
ENDSEC;

DATA;
#8=UNCERTAINTY_MEASURE_WITH_UNIT (LENGTH_MEASURE( 1.000000000000000082E-05 ), #17225, 'distance_accuracy_value', 'NONE');
#99=DIRECTION ( 'NONE',  ( -1.000000000000000000, -0.000000000000000000, -0.000000000000000000 ) ) ;
#130=FACE_BOUND ( 'NONE', #10121, .T. ) ;
#176=DIRECTION ( 'NONE',  ( -1.000000000000000000, -0.000000000000000000, -0.000000000000000000 ) ) ;
#180=DIRECTION ( 'NONE',  ( 0.000000000000000000, 0.000000000000000000, 1.000000000000000000 ) ) ;
#203=ORIENTED_EDGE ( 'NONE', *, *, #11821, .T. ) ;
#238=CARTESIAN_POINT ( 'NONE',  ( 2.500000000000000000, 2.357898499370432166, -2.385244779468109755E-15 ) ) ;
#259=VECTOR ( 'NONE', #12873, 1000.000000000000000 ) ;
#268=LINE ( 'NONE', #7399, #2277 ) ;
#310=EDGE_CURVE ( 'NONE', #18225, #10909, #8683, .T. ) ;
#346=CARTESIAN_POINT ( 'NONE',  ( 34.99999999999999289, 0.000000000000000000, 2.055000000000000160 ) ) ;
#363=AXIS2_PLACEMENT_3D ( 'NONE', #2805, #6567, #23450 ) ;
#405=CARTESIAN_POINT ( 'NONE',  ( 0.2500000000000002220, 0.000000000000000000, 0.000000000000000000 ) ) ;
#408=EDGE_LOOP ( 'NONE', ( #13724, #11220, #22604, #14081, #3269 ) ) ;
#433=CARTESIAN_POINT ( 'NONE',  ( 0.000000000000000000, 1.178949249685213863, -2.042000000000001148 ) ) ;
#487=ORIENTED_EDGE ( 'NONE', *, *, #3373, .T. ) ;
#511=FACE_OUTER_BOUND ( 'NONE', #7299, .T. ) ;
#516=DIRECTION ( 'NONE',  ( -1.000000000000000000, -0.000000000000000000, -0.000000000000000000 ) ) ;
#531=AXIS2_PLACEMENT_3D ( 'NONE', #16784, #7738, #20398 ) ;
#579=CARTESIAN_POINT ( 'NONE',  ( 2.500000000000000000, -1.178949249685218081, -2.041999999999998039 ) ) ;
#593=CARTESIAN_POINT ( 'NONE',  ( 2.500000000000000000, 2.357898499370432166, -2.385244779468109755E-15 ) ) ;
#606=ORIENTED_EDGE ( 'NONE', *, *, #5631, .F. ) ;
#715=DIRECTION ( 'NONE',  ( 1.000000000000000000, 0.000000000000000000, 0.000000000000000000 ) ) ;
#820=ADVANCED_FACE ( 'NONE', ( #17468 ), #12087, .T. ) ;
#855=DIRECTION ( 'NONE',  ( -1.000000000000000000, -0.000000000000000000, -0.000000000000000000 ) ) ;
#867=FACE_OUTER_BOUND ( 'NONE', #11588, .T. ) ;
#893=DIRECTION ( 'NONE',  ( -1.000000000000000000, -0.000000000000000000, -0.000000000000000000 ) ) ;
#934=ORIENTED_EDGE ( 'NONE', *, *, #20472, .F. ) ;
#936=ADVANCED_FACE ( 'NONE', ( #18395 ), #22829, .T. ) ;
#964=CLOSED_SHELL ( 'NONE', ( #4303, #1614, #4833, #820, #19092, #13292, #16891, #6525, #17781, #936, #12661, #23313, #19770, #2931, #21369, #16177, #3125, #20181, #11405, #2100, #13635, #20040, #9767, #13206, #11995, #1311, #13323 ) ) ;
#983=EDGE_LOOP ( 'NONE', ( #16297, #10058, #10495 ) ) ;
#1046=EDGE_CURVE ( 'NONE', #4892, #22378, #4610, .T. ) ;
#1054=LINE ( 'NONE', #19399, #20423 ) ;
#1069=EDGE_LOOP ( 'NONE', ( #487, #5225, #6200, #6955 ) ) ;
#1084=AXIS2_PLACEMENT_3D ( 'NONE', #6713, #12312, #4901 ) ;
#1089=ORIENTED_EDGE ( 'NONE', *, *, #14740, .T. ) ;
#1109=ORIENTED_EDGE ( 'NONE', *, *, #19459, .F. ) ;
#1111=AXIS2_PLACEMENT_3D ( 'NONE', #3066, #8523, #15764 ) ;
#1113=STYLED_ITEM ( 'NONE', ( #18904 ), #6409 ) ;
#1126=DIRECTION ( 'NONE',  ( 0.000000000000000000, 0.000000000000000000, 1.000000000000000000 ) ) ;
#1133=ORIENTED_EDGE ( 'NONE', *, *, #9813, .T. ) ;
#1137=ORIENTED_EDGE ( 'NONE', *, *, #6971, .F. ) ;
#1159=DIRECTION ( 'NONE',  ( -0.000000000000000000, 1.103561164596346103E-15, 1.000000000000000000 ) ) ;
#1189=ORIENTED_EDGE ( 'NONE', *, *, #22007, .T. ) ;
#1194=DIRECTION ( 'NONE',  ( 0.000000000000000000, -0.4999999999999992228, 0.8660254037844390407 ) ) ;
#1265=ORIENTED_EDGE ( 'NONE', *, *, #3366, .F. ) ;
#1297=DIRECTION ( 'NONE',  ( -1.000000000000000000, -0.000000000000000000, -0.000000000000000000 ) ) ;
#1298=CARTESIAN_POINT ( 'NONE',  ( 2.500000000000000000, 2.500728763858895382E-16, -2.041999999999999815 ) ) ;
#1311=ADVANCED_FACE ( 'NONE', ( #20749 ), #18810, .F. ) ;
#1351=AXIS2_PLACEMENT_3D ( 'NONE', #11749, #715, #6029 ) ;
#1375=DIRECTION ( 'NONE',  ( 0.000000000000000000, 0.000000000000000000, -1.000000000000000000 ) ) ;
#1450=ORIENTED_EDGE ( 'NONE', *, *, #2275, .F. ) ;
#1468=CARTESIAN_POINT ( 'NONE',  ( 2.500000000000000000, 2.357898499370432166, -2.385244779468109755E-15 ) ) ;
#1551=AXIS2_PLACEMENT_3D ( 'NONE', #6724, #5046, #6611 ) ;
#1573=ORIENTED_EDGE ( 'NONE', *, *, #16696, .T. ) ;
#1614=ADVANCED_FACE ( 'NONE', ( #16516 ), #16777, .T. ) ;
#1636=ORIENTED_EDGE ( 'NONE', *, *, #15712, .T. ) ;
#1721=DIRECTION ( 'NONE',  ( 0.000000000000000000, 0.000000000000000000, 1.000000000000000000 ) ) ;
#1733=EDGE_CURVE ( 'NONE', #12392, #6476, #21523, .T. ) ;
#1763=VERTEX_POINT ( 'NONE', #3936 ) ;
#1878=ORIENTED_EDGE ( 'NONE', *, *, #3277, .T. ) ;
#1904=VECTOR ( 'NONE', #5428, 1000.000000000000000 ) ;
#1917=UNCERTAINTY_MEASURE_WITH_UNIT (LENGTH_MEASURE( 1.000000000000000082E-05 ), #22409, 'distance_accuracy_value', 'NONE');
#1921=LINE ( 'NONE', #8945, #22502 ) ;
#1984=CARTESIAN_POINT ( 'NONE',  ( 0.2500000000000002220, 4.898587196589412829E-16, -4.000000000000000000 ) ) ;
#2038=DIRECTION ( 'NONE',  ( 0.000000000000000000, 0.000000000000000000, 1.000000000000000000 ) ) ;
#2070=EDGE_CURVE ( 'NONE', #1763, #22378, #13506, .T. ) ;
#2100=ADVANCED_FACE ( 'NONE', ( #7902 ), #18879, .F. ) ;
#2133=DIRECTION ( 'NONE',  ( 0.000000000000000000, -1.000000000000000000, 0.000000000000000000 ) ) ;
#2227=DIRECTION ( 'NONE',  ( -1.000000000000000000, -0.000000000000000000, -0.000000000000000000 ) ) ;
#2253=DIRECTION ( 'NONE',  ( 1.000000000000000000, 0.000000000000000000, 0.000000000000000000 ) ) ;
#2275=EDGE_CURVE ( 'NONE', #2992, #5216, #9439, .T. ) ;
#2277=VECTOR ( 'NONE', #516, 1000.000000000000000 ) ;
#2297=CARTESIAN_POINT ( 'NONE',  ( 5.200000000000002842, 0.000000000000000000, 2.500000000000000444 ) ) ;
#2312=FACE_BOUND ( 'NONE', #23205, .T. ) ;
#2321=CARTESIAN_POINT ( 'NONE',  ( 2.500000000000000000, 2.253471898105738645E-15, 2.041999999999999815 ) ) ;
#2325=DIRECTION ( 'NONE',  ( 0.000000000000000000, -0.4999999999999991118, 0.8660254037844390407 ) ) ;
#2402=VERTEX_POINT ( 'NONE', #12876 ) ;
#2496=DIRECTION ( 'NONE',  ( -1.000000000000000000, -0.000000000000000000, -0.000000000000000000 ) ) ;
#2523=VECTOR ( 'NONE', #1194, 1000.000000000000114 ) ;
#2536=CARTESIAN_POINT ( 'NONE',  ( 2.500000000000000000, 1.178949249685218081, 2.041999999999998483 ) ) ;
#2545=DIRECTION ( 'NONE',  ( -0.000000000000000000, 0.000000000000000000, 1.000000000000000000 ) ) ;
#2620=VECTOR ( 'NONE', #3115, 1000.000000000000114 ) ;
#2639=EDGE_CURVE ( 'NONE', #18956, #2402, #3052, .T. ) ;
#2648=EDGE_CURVE ( 'NONE', #7824, #6807, #268, .T. ) ;
#2672=AXIS2_PLACEMENT_3D ( 'NONE', #9268, #7797, #16629 ) ;
#2724=CARTESIAN_POINT ( 'NONE',  ( 0.000000000000000000, 5.051668046482832750E-16, -4.000000000000000000 ) ) ;
#2755=ORIENTED_EDGE ( 'NONE', *, *, #2275, .T. ) ;
#2797=CARTESIAN_POINT ( 'NONE',  ( 5.000000000000004441, 5.204748896376250699E-16, -4.250000000000000000 ) ) ;
#2805=CARTESIAN_POINT ( 'NONE',  ( 34.99999999999999289, 0.000000000000000000, 0.000000000000000000 ) ) ;
#2900=EDGE_CURVE ( 'NONE', #10909, #18725, #8073, .T. ) ;
#2931=ADVANCED_FACE ( 'NONE', ( #18787 ), #20773, .T. ) ;
#2960=PLANE ( 'NONE',  #8266 ) ;
#2967=CARTESIAN_POINT ( 'NONE',  ( 5.000000000000002665, 0.000000000000000000, -2.700000000000000622 ) ) ;
#2992=VERTEX_POINT ( 'NONE', #13412 ) ;
#3010=VERTEX_POINT ( 'NONE', #579 ) ;
#3052=CIRCLE ( 'NONE', #23099, 4.250000000000000000 ) ;
#3066=CARTESIAN_POINT ( 'NONE',  ( 2.500000000000000000, 2.357898499370432166, -2.385244779468109755E-15 ) ) ;
#3076=EDGE_CURVE ( 'NONE', #21515, #14004, #19612, .T. ) ;
#3088=DIRECTION ( 'NONE',  ( -1.000000000000000000, -0.000000000000000000, -0.000000000000000000 ) ) ;
#3115=DIRECTION ( 'NONE',  ( -0.5000000000000051070, 1.060575238724903217E-16, -0.8660254037844355990 ) ) ;
#3125=ADVANCED_FACE ( 'NONE', ( #11971 ), #23250, .T. ) ;
#3163=DIRECTION ( 'NONE',  ( 0.000000000000000000, -0.5000000000000009992, -0.8660254037844380415 ) ) ;
#3178=CARTESIAN_POINT ( 'NONE',  ( 0.000000000000000000, -1.178949249685218081, -2.041999999999998039 ) ) ;
#3240=VECTOR ( 'NONE', #22984, 1000.000000000000000 ) ;
#3269=ORIENTED_EDGE ( 'NONE', *, *, #21529, .T. ) ;
#3277=EDGE_CURVE ( 'NONE', #10884, #4892, #15987, .T. ) ;
#3295=ORIENTED_EDGE ( 'NONE', *, *, #7592, .F. ) ;
#3308=AXIS2_PLACEMENT_3D ( 'NONE', #10082, #8003, #5835 ) ;
#3366=EDGE_CURVE ( 'NONE', #9294, #6807, #18457, .T. ) ;
#3373=EDGE_CURVE ( 'NONE', #6031, #14121, #4598, .T. ) ;
#3376=DIRECTION ( 'NONE',  ( -1.000000000000000000, -0.000000000000000000, -0.000000000000000000 ) ) ;
#3422=DIRECTION ( 'NONE',  ( 1.000000000000000000, 0.000000000000000000, 0.000000000000000000 ) ) ;
#3452=EDGE_CURVE ( 'NONE', #14004, #21515, #19234, .T. ) ;
#3463=ORIENTED_EDGE ( 'NONE', *, *, #2648, .T. ) ;
#3501=CARTESIAN_POINT ( 'NONE',  ( 2.500000000000000000, 0.000000000000000000, 0.000000000000000000 ) ) ;
#3620=ORIENTED_EDGE ( 'NONE', *, *, #21014, .T. ) ;
#3769=DIRECTION ( 'NONE',  ( 1.000000000000000000, 0.000000000000000000, 0.000000000000000000 ) ) ;
#3782=DIRECTION ( 'NONE',  ( 0.000000000000000000, 0.5000000000000011102, 0.8660254037844380415 ) ) ;
#3842=VECTOR ( 'NONE', #9547, 1000.000000000000000 ) ;
#3850=MANIFOLD_SOLID_BREP ( 'Hex', #964 ) ;
#3888=ORIENTED_EDGE ( 'NONE', *, *, #10067, .F. ) ;
#3936=CARTESIAN_POINT ( 'NONE',  ( 0.000000000000000000, 1.178949249685213863, -2.042000000000001148 ) ) ;
#3946=SHAPE_DEFINITION_REPRESENTATION ( #14440, #8987 ) ;
#4040=AXIS2_PLACEMENT_3D ( 'NONE', #20357, #4503, #16645 ) ;
#4049=DIRECTION ( 'NONE',  ( 0.000000000000000000, 0.000000000000000000, 1.000000000000000000 ) ) ;
#4059=DIRECTION ( 'NONE',  ( 0.000000000000000000, 0.000000000000000000, 1.000000000000000000 ) ) ;
#4082=DIRECTION ( 'NONE',  ( 0.000000000000000000, 0.000000000000000000, -1.000000000000000000 ) ) ;
#4133=CARTESIAN_POINT ( 'NONE',  ( 0.2500000000000002220, 0.000000000000000000, 4.000000000000000000 ) ) ;
#4135=EDGE_CURVE ( 'NONE', #18225, #13331, #10077, .T. ) ;
#4169=CARTESIAN_POINT ( 'NONE',  ( 34.55500000000001393, 0.000000000000000000, 2.500000000000000888 ) ) ;
#4224=VECTOR ( 'NONE', #11098, 1000.000000000000114 ) ;
#4225=CARTESIAN_POINT ( 'NONE',  ( 2.500000000000000000, 1.178949249685213863, -2.042000000000001148 ) ) ;
#4257=EDGE_LOOP ( 'NONE', ( #11830, #6512, #11286 ) ) ;
#4303=ADVANCED_FACE ( 'NONE', ( #14751 ), #15252, .F. ) ;
#4400=AXIS2_PLACEMENT_3D ( 'NONE', #6945, #3422, #1375 ) ;
#4453=EDGE_CURVE ( 'NONE', #2402, #18956, #15645, .T. ) ;
#4503=DIRECTION ( 'NONE',  ( -1.000000000000000000, -0.000000000000000000, -0.000000000000000000 ) ) ;
#4524=EDGE_LOOP ( 'NONE', ( #7154, #12284, #17273, #5472, #3620 ) ) ;
#4542=FACE_OUTER_BOUND ( 'NONE', #22128, .T. ) ;
#4590=AXIS2_PLACEMENT_3D ( 'NONE', #21590, #6848, #21810 ) ;
#4598=CIRCLE ( 'NONE', #363, 2.055000000000000160 ) ;
#4610=LINE ( 'NONE', #23061, #7943 ) ;
#4657=ORIENTED_EDGE ( 'NONE', *, *, #3373, .F. ) ;
#4665=ORIENTED_EDGE ( 'NONE', *, *, #5661, .F. ) ;
#4699=LINE ( 'NONE', #9784, #21101 ) ;
#4734=DIRECTION ( 'NONE',  ( 0.000000000000000000, 0.000000000000000000, -1.000000000000000000 ) ) ;
#4750=LINE ( 'NONE', #19586, #22253 ) ;
#4765=CIRCLE ( 'NONE', #14812, 2.500000000000000444 ) ;
#4833=ADVANCED_FACE ( 'NONE', ( #7910 ), #12228, .F. ) ;
#4892=VERTEX_POINT ( 'NONE', #6450 ) ;
#4901=DIRECTION ( 'NONE',  ( 0.000000000000000000, 0.000000000000000000, 1.000000000000000000 ) ) ;
#5046=DIRECTION ( 'NONE',  ( -1.000000000000000000, -0.000000000000000000, -0.000000000000000000 ) ) ;
#5138=DIRECTION ( 'NONE',  ( -1.000000000000000000, -0.000000000000000000, -0.000000000000000000 ) ) ;
#5216=VERTEX_POINT ( 'NONE', #2321 ) ;
#5225=ORIENTED_EDGE ( 'NONE', *, *, #15117, .T. ) ;
#5230=EDGE_CURVE ( 'NONE', #20797, #21004, #13779, .T. ) ;
#5245=DIRECTION ( 'NONE',  ( -1.000000000000000000, -0.000000000000000000, -0.000000000000000000 ) ) ;
#5274=FACE_OUTER_BOUND ( 'NONE', #9419, .T. ) ;
#5361=DIRECTION ( 'NONE',  ( 0.000000000000000000, 0.000000000000000000, 1.000000000000000000 ) ) ;
#5370=CIRCLE ( 'NONE', #21941, 2.041999999999999815 ) ;
#5391=CARTESIAN_POINT ( 'NONE',  ( 2.500000000000000000, -1.178949249685213863, 2.042000000000001148 ) ) ;
#5428=DIRECTION ( 'NONE',  ( 0.000000000000000000, 1.000000000000000000, -1.103561164596346103E-15 ) ) ;
#5472=ORIENTED_EDGE ( 'NONE', *, *, #9405, .T. ) ;
#5571=CONICAL_SURFACE ( 'NONE', #20993, 2.055000000000000160, 0.7853981633974794763 ) ;
#5631=EDGE_CURVE ( 'NONE', #21515, #2402, #19067, .T. ) ;
#5661=EDGE_CURVE ( 'NONE', #21513, #6476, #11502, .T. ) ;
#5678=PLANE ( 'NONE',  #7075 ) ;
#5724=CIRCLE ( 'NONE', #6882, 2.041999999999999815 ) ;
#5782=DIRECTION ( 'NONE',  ( 0.000000000000000000, 0.000000000000000000, -1.000000000000000000 ) ) ;
#5798=AXIS2_PLACEMENT_3D ( 'NONE', #8303, #22894, #21093 ) ;
#5833=ORIENTED_EDGE ( 'NONE', *, *, #17205, .F. ) ;
#5835=DIRECTION ( 'NONE',  ( 0.000000000000000000, 0.000000000000000000, -1.000000000000000000 ) ) ;
#5864=CARTESIAN_POINT ( 'NONE',  ( 2.500000000000000000, -2.357898499370431722, 2.818925648462311528E-15 ) ) ;
#5875=DIRECTION ( 'NONE',  ( -1.000000000000000000, -0.000000000000000000, -0.000000000000000000 ) ) ;
#5903=LINE ( 'NONE', #238, #10323 ) ;
#6029=DIRECTION ( 'NONE',  ( 0.000000000000000000, 0.000000000000000000, 1.000000000000000000 ) ) ;
#6031=VERTEX_POINT ( 'NONE', #346 ) ;
#6060=EDGE_LOOP ( 'NONE', ( #6871, #1089, #8119, #10717, #22180 ) ) ;
#6133=VERTEX_POINT ( 'NONE', #20985 ) ;
#6147=VECTOR ( 'NONE', #21202, 1000.000000000000000 ) ;
#6200=ORIENTED_EDGE ( 'NONE', *, *, #16137, .F. ) ;
#6334=DIRECTION ( 'NONE',  ( 0.000000000000000000, 0.000000000000000000, -1.000000000000000000 ) ) ;
#6347=DIRECTION ( 'NONE',  ( -1.000000000000000000, -0.000000000000000000, -0.000000000000000000 ) ) ;
#6352=PLANE ( 'NONE',  #17304 ) ;
#6376=DIRECTION ( 'NONE',  ( -1.000000000000000000, -0.000000000000000000, -0.000000000000000000 ) ) ;
#6405=EDGE_LOOP ( 'NONE', ( #20168, #12479, #934, #4665, #13030 ) ) ;
#6409=ADVANCED_BREP_SHAPE_REPRESENTATION ( '', ( #3850, #11210 ), #18837 ) ;
#6417=AXIS2_PLACEMENT_3D ( 'NONE', #18748, #13148, #3782 ) ;
#6426=LINE ( 'NONE', #6556, #13133 ) ;
#6449=DIRECTION ( 'NONE',  ( -1.000000000000000000, -0.000000000000000000, -0.000000000000000000 ) ) ;
#6450=CARTESIAN_POINT ( 'NONE',  ( 0.000000000000000000, -2.357898499370431722, 2.818925648462311528E-15 ) ) ;
#6476=VERTEX_POINT ( 'NONE', #18761 ) ;
#6498=VECTOR ( 'NONE', #2227, 1000.000000000000000 ) ;
#6512=ORIENTED_EDGE ( 'NONE', *, *, #2900, .F. ) ;
#6525=ADVANCED_FACE ( 'NONE', ( #7551 ), #22513, .T. ) ;
#6556=CARTESIAN_POINT ( 'NONE',  ( 2.500000000000000000, -1.178949249685218081, -2.041999999999998039 ) ) ;
#6558=AXIS2_PLACEMENT_3D ( 'NONE', #4133, #9477, #18871 ) ;
#6567=DIRECTION ( 'NONE',  ( -1.000000000000000000, -0.000000000000000000, -0.000000000000000000 ) ) ;
#6611=DIRECTION ( 'NONE',  ( 0.000000000000000000, 0.000000000000000000, 1.000000000000000000 ) ) ;
#6668=AXIS2_PLACEMENT_3D ( 'NONE', #12101, #6376, #14015 ) ;
#6675=ORIENTED_EDGE ( 'NONE', *, *, #18180, .F. ) ;
#6713=CARTESIAN_POINT ( 'NONE',  ( 34.55500000000001393, 0.000000000000000000, 0.000000000000000000 ) ) ;
#6724=CARTESIAN_POINT ( 'NONE',  ( 5.000000000000004441, 0.000000000000000000, 0.000000000000000000 ) ) ;
#6765=VECTOR ( 'NONE', #19203, 1000.000000000000114 ) ;
#6807=VERTEX_POINT ( 'NONE', #2297 ) ;
#6848=DIRECTION ( 'NONE',  ( -1.000000000000000000, -0.000000000000000000, -0.000000000000000000 ) ) ;
#6871=ORIENTED_EDGE ( 'NONE', *, *, #15712, .F. ) ;
#6882=AXIS2_PLACEMENT_3D ( 'NONE', #18776, #5875, #4049 ) ;
#6945=CARTESIAN_POINT ( 'NONE',  ( 2.500000000000000000, 2.357898499370432166, -2.385244779468109755E-15 ) ) ;
#6955=ORIENTED_EDGE ( 'NONE', *, *, #23582, .F. ) ;
#6966=ORIENTED_EDGE ( 'NONE', *, *, #17747, .F. ) ;
#6971=EDGE_CURVE ( 'NONE', #6476, #14316, #18576, .T. ) ;
#6990=LINE ( 'NONE', #1298, #2620 ) ;
#7044=CIRCLE ( 'NONE', #6668, 2.041999999999999815 ) ;
#7075=AXIS2_PLACEMENT_3D ( 'NONE', #11151, #20162, #11030 ) ;
#7154=ORIENTED_EDGE ( 'NONE', *, *, #3277, .F. ) ;
#7164=CIRCLE ( 'NONE', #17599, 2.500000000000000888 ) ;
#7284=( GEOMETRIC_REPRESENTATION_CONTEXT ( 3 ) GLOBAL_UNCERTAINTY_ASSIGNED_CONTEXT ( ( #8 ) ) GLOBAL_UNIT_ASSIGNED_CONTEXT ( ( #17225, #11826, #19136 ) ) REPRESENTATION_CONTEXT ( 'NONE', 'WORKASPACE' ) );
#7299=EDGE_LOOP ( 'NONE', ( #9302, #13594 ) ) ;
#7314=DIRECTION ( 'NONE',  ( 0.000000000000000000, -1.224646799147353454E-16, 1.000000000000000000 ) ) ;
#7399=CARTESIAN_POINT ( 'NONE',  ( -31.74999999999995737, 0.000000000000000000, 2.500000000000000444 ) ) ;
#7415=CARTESIAN_POINT ( 'NONE',  ( 2.500000000000000000, -1.178949249685213863, 2.042000000000001148 ) ) ;
#7491=AXIS2_PLACEMENT_3D ( 'NONE', #10324, #8377, #17547 ) ;
#7551=FACE_OUTER_BOUND ( 'NONE', #11244, .T. ) ;
#7589=PRODUCT_DEFINITION_CONTEXT ( 'detailed design', #14786, 'design' ) ;
#7592=EDGE_CURVE ( 'NONE', #14316, #2992, #7044, .T. ) ;
#7594=EDGE_LOOP ( 'NONE', ( #19713, #22218, #18798, #13305 ) ) ;
#7618=DIRECTION ( 'NONE',  ( 0.000000000000000000, 1.224646799147353207E-16, 1.000000000000000000 ) ) ;
#7679=AXIS2_PLACEMENT_3D ( 'NONE', #14075, #19345, #15745 ) ;
#7710=DIRECTION ( 'NONE',  ( 0.000000000000000000, 0.000000000000000000, -1.000000000000000000 ) ) ;
#7720=VECTOR ( 'NONE', #9919, 1000.000000000000000 ) ;
#7738=DIRECTION ( 'NONE',  ( 0.000000000000000000, -1.287488025362403787E-15, -1.000000000000000000 ) ) ;
#7742=CARTESIAN_POINT ( 'NONE',  ( -31.74999999999995737, 5.204748896376250699E-16, -4.250000000000000000 ) ) ;
#7747=CARTESIAN_POINT ( 'NONE',  ( 0.000000000000000000, -1.178949249685213863, 2.042000000000001148 ) ) ;
#7797=DIRECTION ( 'NONE',  ( 1.000000000000000000, 0.000000000000000000, 0.000000000000000000 ) ) ;
#7816=DIRECTION ( 'NONE',  ( 0.000000000000000000, 0.000000000000000000, 1.000000000000000000 ) ) ;
#7822=CARTESIAN_POINT ( 'NONE',  ( 2.500000000000000000, 2.357898499370432166, -2.385244779468109755E-15 ) ) ;
#7823=DIRECTION ( 'NONE',  ( -1.000000000000000000, -0.000000000000000000, -0.000000000000000000 ) ) ;
#7824=VERTEX_POINT ( 'NONE', #4169 ) ;
#7869=PLANE ( 'NONE',  #22606 ) ;
#7884=DIRECTION ( 'NONE',  ( -0.000000000000000000, 0.8660254037844391517, 0.4999999999999991673 ) ) ;
#7902=FACE_OUTER_BOUND ( 'NONE', #15321, .T. ) ;
#7910=FACE_OUTER_BOUND ( 'NONE', #12309, .T. ) ;
#7943=VECTOR ( 'NONE', #12027, 1000.000000000000000 ) ;
#8003=DIRECTION ( 'NONE',  ( -1.000000000000000000, -0.000000000000000000, -0.000000000000000000 ) ) ;
#8008=FACE_OUTER_BOUND ( 'NONE', #408, .T. ) ;
#8065=DIRECTION ( 'NONE',  ( -1.000000000000000000, -0.000000000000000000, -0.000000000000000000 ) ) ;
#8069=AXIS2_PLACEMENT_3D ( 'NONE', #17188, #21285, #4734 ) ;
#8073=LINE ( 'NONE', #7822, #13503 ) ;
#8092=( GEOMETRIC_REPRESENTATION_CONTEXT ( 3 ) GLOBAL_UNCERTAINTY_ASSIGNED_CONTEXT ( ( #19164 ) ) GLOBAL_UNIT_ASSIGNED_CONTEXT ( ( #12282, #17548, #12771 ) ) REPRESENTATION_CONTEXT ( 'NONE', 'WORKASPACE' ) );
#8119=ORIENTED_EDGE ( 'NONE', *, *, #15952, .T. ) ;
#8141=CARTESIAN_POINT ( 'NONE',  ( 0.000000000000000000, 0.000000000000000000, 0.000000000000000000 ) ) ;
#8167=CARTESIAN_POINT ( 'NONE',  ( 5.200000000000002842, 0.000000000000000000, 0.000000000000000000 ) ) ;
#8247=DIRECTION ( 'NONE',  ( -1.000000000000000000, -0.000000000000000000, -0.000000000000000000 ) ) ;
#8251=VECTOR ( 'NONE', #7823, 1000.000000000000000 ) ;
#8266=AXIS2_PLACEMENT_3D ( 'NONE', #13554, #10133, #15681 ) ;
#8281=FACE_OUTER_BOUND ( 'NONE', #4257, .T. ) ;
#8288=CARTESIAN_POINT ( 'NONE',  ( 5.000000000000000888, 0.000000000000000000, 0.000000000000000000 ) ) ;
#8289=LINE ( 'NONE', #17570, #14679 ) ;
#8303=CARTESIAN_POINT ( 'NONE',  ( 2.500000000000000000, -1.178949249685213863, 2.042000000000001148 ) ) ;
#8377=DIRECTION ( 'NONE',  ( -1.000000000000000000, -0.000000000000000000, -0.000000000000000000 ) ) ;
#8388=LINE ( 'NONE', #21072, #3240 ) ;
#8523=DIRECTION ( 'NONE',  ( 1.000000000000000000, 0.000000000000000000, 0.000000000000000000 ) ) ;
#8555=LINE ( 'NONE', #19760, #19224 ) ;
#8601=APPLICATION_CONTEXT ( 'automotive_design' ) ;
#8615=CARTESIAN_POINT ( 'NONE',  ( 0.000000000000000000, -1.178949249685213863, 2.042000000000001148 ) ) ;
#8621=CARTESIAN_POINT ( 'NONE',  ( 0.000000000000000000, 2.357898499370432166, -2.385244779468109755E-15 ) ) ;
#8679=DIRECTION ( 'NONE',  ( 0.000000000000000000, 0.000000000000000000, 1.000000000000000000 ) ) ;
#8683=LINE ( 'NONE', #12351, #2523 ) ;
#8794=CYLINDRICAL_SURFACE ( 'NONE', #4590, 4.250000000000000000 ) ;
#8825=AXIS2_PLACEMENT_3D ( 'NONE', #8141, #8247, #19444 ) ;
#8878=ORIENTED_EDGE ( 'NONE', *, *, #3076, .T. ) ;
#8890=CARTESIAN_POINT ( 'NONE',  ( 2.500000000000000000, 2.357898499370432166, -2.385244779468109755E-15 ) ) ;
#8945=CARTESIAN_POINT ( 'NONE',  ( 2.500000000000000000, 2.357898499370432166, -2.385244779468109755E-15 ) ) ;
#8964=FACE_OUTER_BOUND ( 'NONE', #22981, .T. ) ;
#8987=SHAPE_REPRESENTATION ( 'socket head cap screw_iso_ISO 4762 M5 x 30 - 22N', ( #11210 ), #18837 ) ;
#9045=ORIENTED_EDGE ( 'NONE', *, *, #9179, .F. ) ;
#9082=ORIENTED_EDGE ( 'NONE', *, *, #3452, .T. ) ;
#9179=EDGE_CURVE ( 'NONE', #21004, #20797, #17637, .T. ) ;
#9194=VECTOR ( 'NONE', #16718, 1000.000000000000114 ) ;
#9268=CARTESIAN_POINT ( 'NONE',  ( 34.99999999999999289, 2.055000000000000160, 0.000000000000000000 ) ) ;
#9277=LINE ( 'NONE', #10877, #4224 ) ;
#9294=VERTEX_POINT ( 'NONE', #20311 ) ;
#9302=ORIENTED_EDGE ( 'NONE', *, *, #13501, .T. ) ;
#9342=EDGE_LOOP ( 'NONE', ( #14179, #17360, #12381, #10186, #11137 ) ) ;
#9351=CARTESIAN_POINT ( 'NONE',  ( 2.500000000000000000, -2.357898499370431722, 2.818925648462311528E-15 ) ) ;
#9405=EDGE_CURVE ( 'NONE', #2992, #12275, #18274, .T. ) ;
#9419=EDGE_LOOP ( 'NONE', ( #606, #8878, #11350, #14778 ) ) ;
#9428=FACE_OUTER_BOUND ( 'NONE', #6405, .T. ) ;
#9439=CIRCLE ( 'NONE', #7491, 2.041999999999999815 ) ;
#9457=EDGE_CURVE ( 'NONE', #18956, #11863, #18905, .T. ) ;
#9462=ORIENTED_EDGE ( 'NONE', *, *, #2639, .F. ) ;
#9473=CARTESIAN_POINT ( 'NONE',  ( 0.000000000000000000, 0.000000000000000000, 0.000000000000000000 ) ) ;
#9477=DIRECTION ( 'NONE',  ( 0.000000000000000000, -1.000000000000000000, 0.000000000000000000 ) ) ;
#9547=DIRECTION ( 'NONE',  ( -1.000000000000000000, -0.000000000000000000, -0.000000000000000000 ) ) ;
#9556=AXIS2_PLACEMENT_3D ( 'NONE', #12277, #17665, #1126 ) ;
#9601=AXIS2_PLACEMENT_3D ( 'NONE', #19151, #15454, #4059 ) ;
#9615=CARTESIAN_POINT ( 'NONE',  ( 2.500000000000000000, -2.357898499370431722, 2.818925648462311528E-15 ) ) ;
#9700=ORIENTED_EDGE ( 'NONE', *, *, #5230, .T. ) ;
#9745=LINE ( 'NONE', #19257, #6147 ) ;
#9767=ADVANCED_FACE ( 'NONE', ( #14655 ), #19709, .F. ) ;
#9784=CARTESIAN_POINT ( 'NONE',  ( 2.500000000000000000, -2.357898499370431722, 2.818925648462311528E-15 ) ) ;
#9809=DIRECTION ( 'NONE',  ( 0.000000000000000000, 1.000000000000000000, -1.224646799147353207E-16 ) ) ;
#9813=EDGE_CURVE ( 'NONE', #6807, #21004, #21215, .T. ) ;
#9884=DIRECTION ( 'NONE',  ( 0.000000000000000000, 0.000000000000000000, 1.000000000000000000 ) ) ;
#9919=DIRECTION ( 'NONE',  ( 0.000000000000000000, -1.000000000000000000, 1.287488025362403787E-15 ) ) ;
#10023=VECTOR ( 'NONE', #893, 1000.000000000000000 ) ;
#10058=ORIENTED_EDGE ( 'NONE', *, *, #11804, .T. ) ;
#10066=ORIENTED_EDGE ( 'NONE', *, *, #16300, .F. ) ;
#10067=EDGE_CURVE ( 'NONE', #13198, #11863, #21167, .T. ) ;
#10077=LINE ( 'NONE', #19329, #19448 ) ;
#10082=CARTESIAN_POINT ( 'NONE',  ( 5.000000000000000888, 0.000000000000000000, 0.000000000000000000 ) ) ;
#10098=DIRECTION ( 'NONE',  ( 0.000000000000000000, -0.5000000000000011102, -0.8660254037844379305 ) ) ;
#10104=CYLINDRICAL_SURFACE ( 'NONE', #12757, 2.500000000000000444 ) ;
#10117=FILL_AREA_STYLE_COLOUR ( '', #15034 ) ;
#10121=EDGE_LOOP ( 'NONE', ( #9700, #10167 ) ) ;
#10133=DIRECTION ( 'NONE',  ( 1.000000000000000000, 0.000000000000000000, 0.000000000000000000 ) ) ;
#10167=ORIENTED_EDGE ( 'NONE', *, *, #9179, .T. ) ;
#10186=ORIENTED_EDGE ( 'NONE', *, *, #2900, .T. ) ;
#10240=DIRECTION ( 'NONE',  ( 0.000000000000000000, 0.000000000000000000, 1.000000000000000000 ) ) ;
#10261=DIRECTION ( 'NONE',  ( 0.000000000000000000, 1.000000000000000000, -1.103561164596346103E-15 ) ) ;
#10323=VECTOR ( 'NONE', #13312, 1000.000000000000114 ) ;
#10324=CARTESIAN_POINT ( 'NONE',  ( 2.500000000000000000, 0.000000000000000000, 0.000000000000000000 ) ) ;
#10332=CARTESIAN_POINT ( 'NONE',  ( -31.74999999999995737, 0.000000000000000000, 0.000000000000000000 ) ) ;
#10385=PRODUCT ( 'socket head cap screw_iso_ISO 4762 M5 x 30 - 22N', 'socket head cap screw_iso_ISO 4762 M5 x 30 - 22N', '', ( #20143 ) ) ;
#10401=ORIENTED_EDGE ( 'NONE', *, *, #9813, .F. ) ;
#10421=CARTESIAN_POINT ( 'NONE',  ( 0.000000000000000000, 0.000000000000000000, 0.000000000000000000 ) ) ;
#10495=ORIENTED_EDGE ( 'NONE', *, *, #14410, .F. ) ;
#10500=DIRECTION ( 'NONE',  ( 1.000000000000000000, 0.000000000000000000, 0.000000000000000000 ) ) ;
#10564=DIRECTION ( 'NONE',  ( 1.000000000000000000, 0.000000000000000000, 0.000000000000000000 ) ) ;
#10590=FACE_OUTER_BOUND ( 'NONE', #1069, .T. ) ;
#10602=EDGE_CURVE ( 'NONE', #21414, #9294, #16722, .T. ) ;
#10616=CARTESIAN_POINT ( 'NONE',  ( 34.99999999999999289, 0.000000000000000000, 0.000000000000000000 ) ) ;
#10667=DIRECTION ( 'NONE',  ( 0.000000000000000000, 0.000000000000000000, 1.000000000000000000 ) ) ;
#10717=ORIENTED_EDGE ( 'NONE', *, *, #14410, .T. ) ;
#10718=CARTESIAN_POINT ( 'NONE',  ( -31.74999999999995737, 3.061616997868383634E-16, -2.500000000000000444 ) ) ;
#10834=AXIS2_PLACEMENT_3D ( 'NONE', #16691, #9809, #7618 ) ;
#10877=CARTESIAN_POINT ( 'NONE',  ( 2.500000000000000000, 0.000000000000000000, 2.041999999999999815 ) ) ;
#10884=VERTEX_POINT ( 'NONE', #7747 ) ;
#10909=VERTEX_POINT ( 'NONE', #15239 ) ;
#10929=LINE ( 'NONE', #23580, #259 ) ;
#10986=EDGE_CURVE ( 'NONE', #2402, #13198, #11785, .T. ) ;
#11030=DIRECTION ( 'NONE',  ( 0.000000000000000000, 0.000000000000000000, -1.000000000000000000 ) ) ;
#11098=DIRECTION ( 'NONE',  ( -0.5000000000000051070, 0.000000000000000000, 0.8660254037844355990 ) ) ;
#11099=EDGE_LOOP ( 'NONE', ( #20644, #1189, #18156, #10066 ) ) ;
#11137=ORIENTED_EDGE ( 'NONE', *, *, #14052, .T. ) ;
#11151=CARTESIAN_POINT ( 'NONE',  ( 5.000000000000000888, 4.250000000000000000, 0.000000000000000000 ) ) ;
#11179=AXIS2_PLACEMENT_3D ( 'NONE', #18063, #23609, #10240 ) ;
#11203=DIRECTION ( 'NONE',  ( 0.000000000000000000, 0.000000000000000000, 1.000000000000000000 ) ) ;
#11210=AXIS2_PLACEMENT_3D ( 'NONE', #9473, #14914, #3769 ) ;
#11220=ORIENTED_EDGE ( 'NONE', *, *, #21014, .F. ) ;
#11244=EDGE_LOOP ( 'NONE', ( #4657, #17847 ) ) ;
#11286=ORIENTED_EDGE ( 'NONE', *, *, #15952, .F. ) ;
#11306=AXIS2_PLACEMENT_3D ( 'NONE', #16404, #99, #14841 ) ;
#11350=ORIENTED_EDGE ( 'NONE', *, *, #20075, .T. ) ;
#11405=ADVANCED_FACE ( 'NONE', ( #9428 ), #18581, .F. ) ;
#11502=LINE ( 'NONE', #4225, #7720 ) ;
#11585=SURFACE_SIDE_STYLE ('',( #15777 ) ) ;
#11588=EDGE_LOOP ( 'NONE', ( #19869, #14356, #1137 ) ) ;
#11615=PRODUCT_DEFINITION_FORMATION_WITH_SPECIFIED_SOURCE ( 'ANY', '', #10385, .NOT_KNOWN. ) ;
#11715=CARTESIAN_POINT ( 'NONE',  ( 2.500000000000000000, 0.000000000000000000, 0.000000000000000000 ) ) ;
#11747=CARTESIAN_POINT ( 'NONE',  ( 2.500000000000000000, 2.357898499370432166, -2.385244779468109755E-15 ) ) ;
#11749=CARTESIAN_POINT ( 'NONE',  ( 0.2500000000000002220, 0.000000000000000000, 0.000000000000000000 ) ) ;
#11785=CIRCLE ( 'NONE', #19057, 0.2500000000000002220 ) ;
#11804=EDGE_CURVE ( 'NONE', #18225, #12392, #1921, .T. ) ;
#11821=EDGE_CURVE ( 'NONE', #6807, #9294, #4765, .T. ) ;
#11826=( NAMED_UNIT ( * ) PLANE_ANGLE_UNIT ( ) SI_UNIT ( $, .RADIAN. ) );
#11830=ORIENTED_EDGE ( 'NONE', *, *, #13093, .T. ) ;
#11860=EDGE_CURVE ( 'NONE', #21513, #1763, #17017, .T. ) ;
#11863=VERTEX_POINT ( 'NONE', #13413 ) ;
#11875=EDGE_LOOP ( 'NONE', ( #15019, #14021, #3463, #203 ) ) ;
#11896=CARTESIAN_POINT ( 'NONE',  ( 2.500000000000000000, -1.178949249685213863, 2.042000000000001148 ) ) ;
#11900=ORIENTED_EDGE ( 'NONE', *, *, #17205, .T. ) ;
#11938=CARTESIAN_POINT ( 'NONE',  ( -31.74999999999995737, 0.000000000000000000, 4.250000000000000000 ) ) ;
#11971=FACE_OUTER_BOUND ( 'NONE', #4524, .T. ) ;
#11995=ADVANCED_FACE ( 'NONE', ( #12094 ), #2960, .F. ) ;
#12027=DIRECTION ( 'NONE',  ( 0.000000000000000000, 0.4999999999999991118, -0.8660254037844391517 ) ) ;
#12080=( NAMED_UNIT ( * ) PLANE_ANGLE_UNIT ( ) SI_UNIT ( $, .RADIAN. ) );
#12087=CYLINDRICAL_SURFACE ( 'NONE', #13726, 4.250000000000000000 ) ;
#12094=FACE_OUTER_BOUND ( 'NONE', #983, .T. ) ;
#12101=CARTESIAN_POINT ( 'NONE',  ( 2.500000000000000000, 0.000000000000000000, 0.000000000000000000 ) ) ;
#12145=CARTESIAN_POINT ( 'NONE',  ( 34.55500000000001393, 3.061616997868384127E-16, -2.500000000000000888 ) ) ;
#12172=FACE_OUTER_BOUND ( 'NONE', #7594, .T. ) ;
#12208=DIRECTION ( 'NONE',  ( 0.000000000000000000, 0.000000000000000000, 1.000000000000000000 ) ) ;
#12224=DIRECTION ( 'NONE',  ( 0.000000000000000000, 0.4999999999999991118, -0.8660254037844391517 ) ) ;
#12228=TOROIDAL_SURFACE ( 'NONE', #19492, 2.700000000000000622, 0.2000000000000000111 ) ;
#12233=ORIENTED_EDGE ( 'NONE', *, *, #10986, .T. ) ;
#12275=VERTEX_POINT ( 'NONE', #9615 ) ;
#12277=CARTESIAN_POINT ( 'NONE',  ( 34.99999999999999289, 0.000000000000000000, 0.000000000000000000 ) ) ;
#12282=( LENGTH_UNIT ( ) NAMED_UNIT ( * ) SI_UNIT ( .MILLI., .METRE. ) );
#12284=ORIENTED_EDGE ( 'NONE', *, *, #16696, .F. ) ;
#12309=EDGE_LOOP ( 'NONE', ( #14693, #1133, #19806, #23341 ) ) ;
#12312=DIRECTION ( 'NONE',  ( -1.000000000000000000, -0.000000000000000000, -0.000000000000000000 ) ) ;
#12345=AXIS2_PLACEMENT_3D ( 'NONE', #13299, #2133, #7710 ) ;
#12351=CARTESIAN_POINT ( 'NONE',  ( 2.500000000000000000, 2.357898499370432166, -2.385244779468109755E-15 ) ) ;
#12381=ORIENTED_EDGE ( 'NONE', *, *, #310, .T. ) ;
#12392=VERTEX_POINT ( 'NONE', #16248 ) ;
#12441=DIRECTION ( 'NONE',  ( 0.000000000000000000, -1.000000000000000000, 1.103561164596346103E-15 ) ) ;
#12479=ORIENTED_EDGE ( 'NONE', *, *, #21529, .F. ) ;
#12578=AXIS2_PLACEMENT_3D ( 'NONE', #3501, #3376, #10667 ) ;
#12654=EDGE_LOOP ( 'NONE', ( #6675, #21243, #1450 ) ) ;
#12661=ADVANCED_FACE ( 'NONE', ( #130, #8964 ), #5678, .T. ) ;
#12684=CIRCLE ( 'NONE', #19550, 2.055000000000000160 ) ;
#12757=AXIS2_PLACEMENT_3D ( 'NONE', #10332, #6449, #2038 ) ;
#12771=( NAMED_UNIT ( * ) SI_UNIT ( $, .STERADIAN. ) SOLID_ANGLE_UNIT ( ) );
#12873=DIRECTION ( 'NONE',  ( -1.000000000000000000, -0.000000000000000000, -0.000000000000000000 ) ) ;
#12876=CARTESIAN_POINT ( 'NONE',  ( 0.2500000000000002220, 5.204748896376250699E-16, -4.250000000000000000 ) ) ;
#13006=FACE_OUTER_BOUND ( 'NONE', #9342, .T. ) ;
#13030=ORIENTED_EDGE ( 'NONE', *, *, #11860, .T. ) ;
#13063=CARTESIAN_POINT ( 'NONE',  ( 2.500000000000000000, -1.178949249685213863, 2.042000000000001148 ) ) ;
#13093=EDGE_CURVE ( 'NONE', #5216, #18725, #8388, .T. ) ;
#13133=VECTOR ( 'NONE', #15739, 1000.000000000000000 ) ;
#13140=VECTOR ( 'NONE', #20643, 1000.000000000000000 ) ;
#13148=DIRECTION ( 'NONE',  ( 0.000000000000000000, 0.8660254037844380415, -0.5000000000000011102 ) ) ;
#13151=AXIS2_PLACEMENT_3D ( 'NONE', #1468, #10564, #14420 ) ;
#13198=VERTEX_POINT ( 'NONE', #2724 ) ;
#13206=ADVANCED_FACE ( 'NONE', ( #8281 ), #18048, .F. ) ;
#13249=VERTEX_POINT ( 'NONE', #23354 ) ;
#13265=CARTESIAN_POINT ( 'NONE',  ( 0.2500000000000002220, 0.000000000000000000, 4.250000000000000000 ) ) ;
#13292=ADVANCED_FACE ( 'NONE', ( #10590 ), #5571, .T. ) ;
#13299=CARTESIAN_POINT ( 'NONE',  ( 5.200000000000002842, 0.000000000000000000, -2.700000000000000622 ) ) ;
#13305=ORIENTED_EDGE ( 'NONE', *, *, #2648, .F. ) ;
#13312=DIRECTION ( 'NONE',  ( 0.000000000000000000, -0.5000000000000011102, -0.8660254037844379305 ) ) ;
#13323=ADVANCED_FACE ( 'NONE', ( #20091 ), #17147, .F. ) ;
#13331=VERTEX_POINT ( 'NONE', #23231 ) ;
#13371=AXIS2_PLACEMENT_3D ( 'NONE', #11747, #22444, #4082 ) ;
#13412=CARTESIAN_POINT ( 'NONE',  ( 2.500000000000000000, -1.768423874527823125, 1.021000000000002128 ) ) ;
#13413=CARTESIAN_POINT ( 'NONE',  ( 0.000000000000000000, 0.000000000000000000, 4.000000000000000000 ) ) ;
#13490=AXIS2_PLACEMENT_3D ( 'NONE', #15919, #10500, #19389 ) ;
#13501=EDGE_CURVE ( 'NONE', #11863, #13198, #18453, .T. ) ;
#13503=VECTOR ( 'NONE', #22424, 1000.000000000000114 ) ;
#13506=LINE ( 'NONE', #433, #13789 ) ;
#13554=CARTESIAN_POINT ( 'NONE',  ( 2.500000000000000000, 2.357898499370432166, -2.385244779468109755E-15 ) ) ;
#13594=ORIENTED_EDGE ( 'NONE', *, *, #10067, .T. ) ;
#13635=ADVANCED_FACE ( 'NONE', ( #867 ), #20801, .F. ) ;
#13642=CARTESIAN_POINT ( 'NONE',  ( 5.000000000000002665, 3.306546357697854226E-16, 2.700000000000000622 ) ) ;
#13724=ORIENTED_EDGE ( 'NONE', *, *, #1046, .F. ) ;
#13726=AXIS2_PLACEMENT_3D ( 'NONE', #19379, #3088, #16135 ) ;
#13779=CIRCLE ( 'NONE', #3308, 2.700000000000000622 ) ;
#13783=ORIENTED_EDGE ( 'NONE', *, *, #9457, .F. ) ;
#13789=VECTOR ( 'NONE', #17083, 1000.000000000000000 ) ;
#13867=CIRCLE ( 'NONE', #12345, 0.2000000000000000944 ) ;
#13939=VECTOR ( 'NONE', #3163, 1000.000000000000114 ) ;
#14004=VERTEX_POINT ( 'NONE', #21016 ) ;
#14015=DIRECTION ( 'NONE',  ( 0.000000000000000000, 0.000000000000000000, 1.000000000000000000 ) ) ;
#14018=ORIENTED_EDGE ( 'NONE', *, *, #14740, .F. ) ;
#14021=ORIENTED_EDGE ( 'NONE', *, *, #16300, .T. ) ;
#14052=EDGE_CURVE ( 'NONE', #18725, #6133, #20768, .T. ) ;
#14075=CARTESIAN_POINT ( 'NONE',  ( 5.200000000000002842, 0.000000000000000000, 0.000000000000000000 ) ) ;
#14080=FACE_OUTER_BOUND ( 'NONE', #11099, .T. ) ;
#14081=ORIENTED_EDGE ( 'NONE', *, *, #17286, .T. ) ;
#14103=DIRECTION ( 'NONE',  ( -0.7071067811865254793, 8.659560562355202797E-17, -0.7071067811865695552 ) ) ;
#14121=VERTEX_POINT ( 'NONE', #20599 ) ;
#14179=ORIENTED_EDGE ( 'NONE', *, *, #20842, .F. ) ;
#14273=DIRECTION ( 'NONE',  ( 0.000000000000000000, -0.5000000000000011102, -0.8660254037844379305 ) ) ;
#14316=VERTEX_POINT ( 'NONE', #15451 ) ;
#14328=DIRECTION ( 'NONE',  ( -0.000000000000000000, 1.000000000000000000, 1.224646799147353207E-16 ) ) ;
#14356=ORIENTED_EDGE ( 'NONE', *, *, #17286, .F. ) ;
#14360=CARTESIAN_POINT ( 'NONE',  ( 2.500000000000000000, 1.178949249685218081, 2.041999999999998483 ) ) ;
#14410=EDGE_CURVE ( 'NONE', #10909, #12392, #5370, .T. ) ;
#14420=DIRECTION ( 'NONE',  ( 0.000000000000000000, 0.000000000000000000, -1.000000000000000000 ) ) ;
#14440=PRODUCT_DEFINITION_SHAPE ( 'NONE', 'NONE',  #20665 ) ;
#14442=CARTESIAN_POINT ( 'NONE',  ( 2.500000000000000000, 0.000000000000000000, 0.000000000000000000 ) ) ;
#14604=EDGE_CURVE ( 'NONE', #10884, #6133, #1054, .T. ) ;
#14607=ORIENTED_EDGE ( 'NONE', *, *, #17831, .T. ) ;
#14655=FACE_OUTER_BOUND ( 'NONE', #12654, .T. ) ;
#14679=VECTOR ( 'NONE', #14103, 1000.000000000000000 ) ;
#14693=ORIENTED_EDGE ( 'NONE', *, *, #11821, .F. ) ;
#14740=EDGE_CURVE ( 'NONE', #13249, #5216, #9277, .T. ) ;
#14751=FACE_OUTER_BOUND ( 'NONE', #17879, .T. ) ;
#14778=ORIENTED_EDGE ( 'NONE', *, *, #2639, .T. ) ;
#14786=APPLICATION_CONTEXT ( 'automotive_design' ) ;
#14812=AXIS2_PLACEMENT_3D ( 'NONE', #22301, #2253, #5782 ) ;
#14841=DIRECTION ( 'NONE',  ( 0.000000000000000000, 0.000000000000000000, 1.000000000000000000 ) ) ;
#14914=DIRECTION ( 'NONE',  ( 0.000000000000000000, 0.000000000000000000, 1.000000000000000000 ) ) ;
#15019=ORIENTED_EDGE ( 'NONE', *, *, #10602, .F. ) ;
#15034=COLOUR_RGB ( '',1.000000000000000000, 0.9490196078431372140, 0.9098039215686274384 ) ;
#15117=EDGE_CURVE ( 'NONE', #14121, #21414, #8289, .T. ) ;
#15150=PLANE ( 'NONE',  #16948 ) ;
#15225=EDGE_LOOP ( 'NONE', ( #9082, #17448, #18752, #16708 ) ) ;
#15239=CARTESIAN_POINT ( 'NONE',  ( 2.500000000000000000, 1.768423874527825124, 1.020999999999998797 ) ) ;
#15252=CONICAL_SURFACE ( 'NONE', #12578, 2.041999999999999815, 1.047197551196591858 ) ;
#15312=ORIENTED_EDGE ( 'NONE', *, *, #14604, .F. ) ;
#15321=EDGE_LOOP ( 'NONE', ( #14607, #16460, #5833, #18908, #16247 ) ) ;
#15424=VECTOR ( 'NONE', #176, 1000.000000000000000 ) ;
#15451=CARTESIAN_POINT ( 'NONE',  ( 2.500000000000000000, -1.768423874527824902, -1.020999999999998353 ) ) ;
#15454=DIRECTION ( 'NONE',  ( -1.000000000000000000, -0.000000000000000000, -0.000000000000000000 ) ) ;
#15540=ORIENTED_EDGE ( 'NONE', *, *, #13093, .F. ) ;
#15551=SHAPE_REPRESENTATION_RELATIONSHIP ( 'NONE' , 'NONE' ,  #8987, #6409 ) ;
#15557=ORIENTED_EDGE ( 'NONE', *, *, #3076, .F. ) ;
#15645=CIRCLE ( 'NONE', #1351, 4.250000000000000000 ) ;
#15681=DIRECTION ( 'NONE',  ( 0.000000000000000000, 0.000000000000000000, -1.000000000000000000 ) ) ;
#15712=EDGE_CURVE ( 'NONE', #13249, #6476, #6990, .T. ) ;
#15739=DIRECTION ( 'NONE',  ( -1.000000000000000000, -0.000000000000000000, -0.000000000000000000 ) ) ;
#15745=DIRECTION ( 'NONE',  ( 0.000000000000000000, 0.000000000000000000, -1.000000000000000000 ) ) ;
#15748=VECTOR ( 'NONE', #23566, 1000.000000000000000 ) ;
#15762=ORIENTED_EDGE ( 'NONE', *, *, #20842, .T. ) ;
#15764=DIRECTION ( 'NONE',  ( 0.000000000000000000, 0.000000000000000000, -1.000000000000000000 ) ) ;
#15776=ORIENTED_EDGE ( 'NONE', *, *, #2070, .F. ) ;
#15777=SURFACE_STYLE_FILL_AREA ( #21318 ) ;
#15833=TOROIDAL_SURFACE ( 'NONE', #13490, 2.700000000000000622, 0.2000000000000000111 ) ;
#15919=CARTESIAN_POINT ( 'NONE',  ( 5.200000000000002842, 0.000000000000000000, 0.000000000000000000 ) ) ;
#15952=EDGE_CURVE ( 'NONE', #5216, #10909, #5724, .T. ) ;
#15987=LINE ( 'NONE', #8615, #13939 ) ;
#16014=DIRECTION ( 'NONE',  ( 0.000000000000000000, 0.000000000000000000, -1.000000000000000000 ) ) ;
#16084=DIRECTION ( 'NONE',  ( -1.000000000000000000, -0.000000000000000000, -0.000000000000000000 ) ) ;
#16127=EDGE_LOOP ( 'NONE', ( #19103, #9462, #18028, #3888 ) ) ;
#16134=CARTESIAN_POINT ( 'NONE',  ( 34.55500000000001393, 0.000000000000000000, 0.000000000000000000 ) ) ;
#16135=DIRECTION ( 'NONE',  ( 0.000000000000000000, 0.000000000000000000, 1.000000000000000000 ) ) ;
#16137=EDGE_CURVE ( 'NONE', #7824, #21414, #18433, .T. ) ;
#16177=ADVANCED_FACE ( 'NONE', ( #4542 ), #6352, .F. ) ;
#16247=ORIENTED_EDGE ( 'NONE', *, *, #4135, .T. ) ;
#16248=CARTESIAN_POINT ( 'NONE',  ( 2.500000000000000000, 1.768423874527822903, -1.021000000000002350 ) ) ;
#16253=DIRECTION ( 'NONE',  ( -1.000000000000000000, -0.000000000000000000, -0.000000000000000000 ) ) ;
#16254=DIRECTION ( 'NONE',  ( 0.000000000000000000, -0.8660254037844390407, -0.4999999999999992784 ) ) ;
#16297=ORIENTED_EDGE ( 'NONE', *, *, #310, .F. ) ;
#16300=EDGE_CURVE ( 'NONE', #21414, #7824, #7164, .T. ) ;
#16404=CARTESIAN_POINT ( 'NONE',  ( 2.500000000000000000, 0.000000000000000000, 0.000000000000000000 ) ) ;
#16460=ORIENTED_EDGE ( 'NONE', *, *, #11860, .F. ) ;
#16516=FACE_OUTER_BOUND ( 'NONE', #17518, .T. ) ;
#16629=DIRECTION ( 'NONE',  ( 0.000000000000000000, 0.000000000000000000, -1.000000000000000000 ) ) ;
#16645=DIRECTION ( 'NONE',  ( 0.000000000000000000, 0.000000000000000000, 1.000000000000000000 ) ) ;
#16691=CARTESIAN_POINT ( 'NONE',  ( 5.200000000000002842, 3.306546357697854226E-16, 2.700000000000000622 ) ) ;
#16696=EDGE_CURVE ( 'NONE', #18832, #10884, #10929, .T. ) ;
#16708=ORIENTED_EDGE ( 'NONE', *, *, #20075, .F. ) ;
#16718=DIRECTION ( 'NONE',  ( 0.000000000000000000, -0.5000000000000009992, -0.8660254037844380415 ) ) ;
#16722=LINE ( 'NONE', #10718, #15424 ) ;
#16777=TOROIDAL_SURFACE ( 'NONE', #4040, 4.000000000000000000, 0.2500000000000000000 ) ;
#16784=CARTESIAN_POINT ( 'NONE',  ( 2.500000000000000000, 1.178949249685213863, -2.042000000000001148 ) ) ;
#16872=ORIENTED_EDGE ( 'NONE', *, *, #14604, .T. ) ;
#16891=ADVANCED_FACE ( 'NONE', ( #2312, #511 ), #7869, .T. ) ;
#16948=AXIS2_PLACEMENT_3D ( 'NONE', #9351, #7884, #2325 ) ;
#17017=LINE ( 'NONE', #20603, #8251 ) ;
#17083=DIRECTION ( 'NONE',  ( 0.000000000000000000, -1.000000000000000000, 1.287488025362403787E-15 ) ) ;
#17147=CONICAL_SURFACE ( 'NONE', #22122, 2.041999999999999815, 1.047197551196591858 ) ;
#17188=CARTESIAN_POINT ( 'NONE',  ( 2.500000000000000000, 2.357898499370432166, -2.385244779468109755E-15 ) ) ;
#17205=EDGE_CURVE ( 'NONE', #12392, #21513, #5903, .T. ) ;
#17225=( LENGTH_UNIT ( ) NAMED_UNIT ( * ) SI_UNIT ( .MILLI., .METRE. ) );
#17273=ORIENTED_EDGE ( 'NONE', *, *, #18180, .T. ) ;
#17278=AXIS2_PLACEMENT_3D ( 'NONE', #8288, #6347, #16014 ) ;
#17286=EDGE_CURVE ( 'NONE', #14316, #3010, #4699, .T. ) ;
#17304=AXIS2_PLACEMENT_3D ( 'NONE', #17824, #1159, #12441 ) ;
#17360=ORIENTED_EDGE ( 'NONE', *, *, #4135, .F. ) ;
#17375=ORIENTED_EDGE ( 'NONE', *, *, #4453, .F. ) ;
#17448=ORIENTED_EDGE ( 'NONE', *, *, #5631, .T. ) ;
#17454=FACE_OUTER_BOUND ( 'NONE', #19404, .T. ) ;
#17468=FACE_OUTER_BOUND ( 'NONE', #15225, .T. ) ;
#17518=EDGE_LOOP ( 'NONE', ( #17375, #12233, #23012, #13783 ) ) ;
#17547=DIRECTION ( 'NONE',  ( 0.000000000000000000, 0.000000000000000000, 1.000000000000000000 ) ) ;
#17548=( NAMED_UNIT ( * ) PLANE_ANGLE_UNIT ( ) SI_UNIT ( $, .RADIAN. ) );
#17570=CARTESIAN_POINT ( 'NONE',  ( 34.99999999999999289, 2.516649172247811061E-16, -2.055000000000000160 ) ) ;
#17599=AXIS2_PLACEMENT_3D ( 'NONE', #16134, #5138, #11203 ) ;
#17631=ORIENTED_EDGE ( 'NONE', *, *, #9405, .F. ) ;
#17637=CIRCLE ( 'NONE', #17278, 2.700000000000000622 ) ;
#17665=DIRECTION ( 'NONE',  ( -1.000000000000000000, -0.000000000000000000, -0.000000000000000000 ) ) ;
#17747=EDGE_CURVE ( 'NONE', #12275, #14316, #4750, .T. ) ;
#17781=ADVANCED_FACE ( 'NONE', ( #14080 ), #19950, .T. ) ;
#17824=CARTESIAN_POINT ( 'NONE',  ( 2.500000000000000000, -1.178949249685213863, 2.042000000000001148 ) ) ;
#17831=EDGE_CURVE ( 'NONE', #13331, #1763, #19236, .T. ) ;
#17838=DIRECTION ( 'NONE',  ( -1.000000000000000000, -0.000000000000000000, -0.000000000000000000 ) ) ;
#17847=ORIENTED_EDGE ( 'NONE', *, *, #22007, .F. ) ;
#17851=CARTESIAN_POINT ( 'NONE',  ( 0.000000000000000000, 0.000000000000000000, 0.000000000000000000 ) ) ;
#17879=EDGE_LOOP ( 'NONE', ( #14018, #1636, #21736, #18210, #2755 ) ) ;
#17980=ORIENTED_EDGE ( 'NONE', *, *, #14052, .F. ) ;
#18028=ORIENTED_EDGE ( 'NONE', *, *, #9457, .T. ) ;
#18048=PLANE ( 'NONE',  #4400 ) ;
#18063=CARTESIAN_POINT ( 'NONE',  ( 5.000000000000004441, 0.000000000000000000, 0.000000000000000000 ) ) ;
#18094=AXIS2_PLACEMENT_3D ( 'NONE', #17851, #1297, #8679 ) ;
#18156=ORIENTED_EDGE ( 'NONE', *, *, #23582, .T. ) ;
#18180=EDGE_CURVE ( 'NONE', #18832, #2992, #21027, .T. ) ;
#18210=ORIENTED_EDGE ( 'NONE', *, *, #7592, .T. ) ;
#18225=VERTEX_POINT ( 'NONE', #593 ) ;
#18263=ORIENTED_EDGE ( 'NONE', *, *, #1733, .F. ) ;
#18274=LINE ( 'NONE', #7415, #9194 ) ;
#18370=DIRECTION ( 'NONE',  ( 1.000000000000000000, 0.000000000000000000, 0.000000000000000000 ) ) ;
#18395=FACE_OUTER_BOUND ( 'NONE', #11875, .T. ) ;
#18433=CIRCLE ( 'NONE', #1084, 2.500000000000000888 ) ;
#18453=CIRCLE ( 'NONE', #8825, 4.000000000000000000 ) ;
#18457=CIRCLE ( 'NONE', #7679, 2.500000000000000444 ) ;
#18468=AXIS2_PLACEMENT_3D ( 'NONE', #8890, #16254, #20092 ) ;
#18476=STYLED_ITEM('',(#23927),#3850);
#18543=ORIENTED_EDGE ( 'NONE', *, *, #3452, .F. ) ;
#18576=CIRCLE ( 'NONE', #11306, 2.041999999999999815 ) ;
#18581=PLANE ( 'NONE',  #531 ) ;
#18705=ORIENTED_EDGE ( 'NONE', *, *, #17831, .F. ) ;
#18725=VERTEX_POINT ( 'NONE', #14360 ) ;
#18748=CARTESIAN_POINT ( 'NONE',  ( 2.500000000000000000, 2.357898499370432166, -2.385244779468109755E-15 ) ) ;
#18752=ORIENTED_EDGE ( 'NONE', *, *, #4453, .T. ) ;
#18761=CARTESIAN_POINT ( 'NONE',  ( 2.500000000000000000, -2.629050547790028551E-15, -2.041999999999999815 ) ) ;
#18776=CARTESIAN_POINT ( 'NONE',  ( 2.500000000000000000, 0.000000000000000000, 0.000000000000000000 ) ) ;
#18787=FACE_OUTER_BOUND ( 'NONE', #16127, .T. ) ;
#18798=ORIENTED_EDGE ( 'NONE', *, *, #3366, .T. ) ;
#18810=PLANE ( 'NONE',  #13371 ) ;
#18832=VERTEX_POINT ( 'NONE', #5391 ) ;
#18837=( GEOMETRIC_REPRESENTATION_CONTEXT ( 3 ) GLOBAL_UNCERTAINTY_ASSIGNED_CONTEXT ( ( #1917 ) ) GLOBAL_UNIT_ASSIGNED_CONTEXT ( ( #22409, #12080, #22990 ) ) REPRESENTATION_CONTEXT ( 'NONE', 'WORKASPACE' ) );
#18871=DIRECTION ( 'NONE',  ( 0.000000000000000000, 0.000000000000000000, -1.000000000000000000 ) ) ;
#18879=PLANE ( 'NONE',  #6417 ) ;
#18904=PRESENTATION_STYLE_ASSIGNMENT (( #22879 ) ) ;
#18905=CIRCLE ( 'NONE', #6558, 0.2500000000000002220 ) ;
#18908=ORIENTED_EDGE ( 'NONE', *, *, #11804, .F. ) ;
#18956=VERTEX_POINT ( 'NONE', #13265 ) ;
#19029=CARTESIAN_POINT ( 'NONE',  ( 2.500000000000000000, 0.000000000000000000, 0.000000000000000000 ) ) ;
#19057=AXIS2_PLACEMENT_3D ( 'NONE', #1984, #14328, #7314 ) ;
#19067=LINE ( 'NONE', #7742, #3842 ) ;
#19080=DIRECTION ( 'NONE',  ( -1.000000000000000000, 0.000000000000000000, -0.000000000000000000 ) ) ;
#19082=CARTESIAN_POINT ( 'NONE',  ( -31.74999999999995737, 0.000000000000000000, 0.000000000000000000 ) ) ;
#19092=ADVANCED_FACE ( 'NONE', ( #12172 ), #10104, .T. ) ;
#19103=ORIENTED_EDGE ( 'NONE', *, *, #10986, .F. ) ;
#19136=( NAMED_UNIT ( * ) SI_UNIT ( $, .STERADIAN. ) SOLID_ANGLE_UNIT ( ) );
#19151=CARTESIAN_POINT ( 'NONE',  ( 0.2500000000000002220, 0.000000000000000000, 0.000000000000000000 ) ) ;
#19164=UNCERTAINTY_MEASURE_WITH_UNIT (LENGTH_MEASURE( 1.000000000000000082E-05 ), #12282, 'distance_accuracy_value', 'NONE');
#19203=DIRECTION ( 'NONE',  ( 0.000000000000000000, -0.5000000000000009992, -0.8660254037844380415 ) ) ;
#19224=VECTOR ( 'NONE', #21341, 1000.000000000000114 ) ;
#19234=CIRCLE ( 'NONE', #11179, 4.250000000000000000 ) ;
#19236=LINE ( 'NONE', #8621, #22643 ) ;
#19257=CARTESIAN_POINT ( 'NONE',  ( 34.99999999999999289, 0.000000000000000000, 2.055000000000000160 ) ) ;
#19282=FACE_OUTER_BOUND ( 'NONE', #21126, .T. ) ;
#19329=CARTESIAN_POINT ( 'NONE',  ( 2.500000000000000000, 2.357898499370432166, -2.385244779468109755E-15 ) ) ;
#19338=CARTESIAN_POINT ( 'NONE',  ( 2.500000000000000000, 1.178949249685213863, -2.042000000000001148 ) ) ;
#19345=DIRECTION ( 'NONE',  ( 1.000000000000000000, 0.000000000000000000, 0.000000000000000000 ) ) ;
#19379=CARTESIAN_POINT ( 'NONE',  ( -31.74999999999995737, 0.000000000000000000, 0.000000000000000000 ) ) ;
#19389=DIRECTION ( 'NONE',  ( 0.000000000000000000, 0.000000000000000000, -1.000000000000000000 ) ) ;
#19399=CARTESIAN_POINT ( 'NONE',  ( 0.000000000000000000, -1.178949249685213863, 2.042000000000001148 ) ) ;
#19404=EDGE_LOOP ( 'NONE', ( #6966, #17631, #3295 ) ) ;
#19444=DIRECTION ( 'NONE',  ( 0.000000000000000000, 0.000000000000000000, 1.000000000000000000 ) ) ;
#19448=VECTOR ( 'NONE', #16084, 1000.000000000000000 ) ;
#19459=EDGE_CURVE ( 'NONE', #18832, #5216, #20368, .T. ) ;
#19463=DIRECTION ( 'NONE',  ( 0.000000000000000000, 0.4999999999999991118, -0.8660254037844391517 ) ) ;
#19492=AXIS2_PLACEMENT_3D ( 'NONE', #8167, #22507, #6334 ) ;
#19550=AXIS2_PLACEMENT_3D ( 'NONE', #10616, #17838, #12208 ) ;
#19584=EDGE_CURVE ( 'NONE', #9294, #20797, #13867, .T. ) ;
#19586=CARTESIAN_POINT ( 'NONE',  ( 2.500000000000000000, -2.357898499370431722, 2.818925648462311528E-15 ) ) ;
#19600=PLANE ( 'NONE',  #1111 ) ;
#19612=CIRCLE ( 'NONE', #1551, 4.250000000000000000 ) ;
#19709=PLANE ( 'NONE',  #13151 ) ;
#19713=ORIENTED_EDGE ( 'NONE', *, *, #16137, .T. ) ;
#19760=CARTESIAN_POINT ( 'NONE',  ( 0.000000000000000000, 2.357898499370432166, -2.385244779468109755E-15 ) ) ;
#19770=ADVANCED_FACE ( 'NONE', ( #19282 ), #15833, .F. ) ;
#19806=ORIENTED_EDGE ( 'NONE', *, *, #5230, .F. ) ;
#19869=ORIENTED_EDGE ( 'NONE', *, *, #20472, .T. ) ;
#19950=CONICAL_SURFACE ( 'NONE', #9556, 2.055000000000000160, 0.7853981633974794763 ) ;
#20012=MECHANICAL_DESIGN_GEOMETRIC_PRESENTATION_REPRESENTATION('',(#18476),#8092);
#20040=ADVANCED_FACE ( 'NONE', ( #17454 ), #19600, .F. ) ;
#20075=EDGE_CURVE ( 'NONE', #14004, #18956, #23114, .T. ) ;
#20091=FACE_OUTER_BOUND ( 'NONE', #6060, .T. ) ;
#20092=DIRECTION ( 'NONE',  ( 0.000000000000000000, 0.4999999999999992784, -0.8660254037844390407 ) ) ;
#20143=PRODUCT_CONTEXT ( 'NONE', #8601, 'mechanical' ) ;
#20162=DIRECTION ( 'NONE',  ( 1.000000000000000000, 0.000000000000000000, 0.000000000000000000 ) ) ;
#20168=ORIENTED_EDGE ( 'NONE', *, *, #2070, .T. ) ;
#20181=ADVANCED_FACE ( 'NONE', ( #8008 ), #15150, .T. ) ;
#20311=CARTESIAN_POINT ( 'NONE',  ( 5.200000000000002842, 3.061616997868383634E-16, -2.500000000000000444 ) ) ;
#20357=CARTESIAN_POINT ( 'NONE',  ( 0.2500000000000002220, 0.000000000000000000, 0.000000000000000000 ) ) ;
#20368=LINE ( 'NONE', #13063, #1904 ) ;
#20398=DIRECTION ( 'NONE',  ( 0.000000000000000000, 1.000000000000000000, -1.287488025362403787E-15 ) ) ;
#20423=VECTOR ( 'NONE', #10261, 1000.000000000000000 ) ;
#20472=EDGE_CURVE ( 'NONE', #6476, #3010, #23672, .T. ) ;
#20599=CARTESIAN_POINT ( 'NONE',  ( 34.99999999999999289, 2.789133085058097101E-16, -2.055000000000000160 ) ) ;
#20603=CARTESIAN_POINT ( 'NONE',  ( 2.500000000000000000, 1.178949249685213863, -2.042000000000001148 ) ) ;
#20643=DIRECTION ( 'NONE',  ( -1.000000000000000000, -0.000000000000000000, -0.000000000000000000 ) ) ;
#20644=ORIENTED_EDGE ( 'NONE', *, *, #15117, .F. ) ;
#20665=PRODUCT_DEFINITION ( 'UNKNOWN', '', #11615, #7589 ) ;
#20749=FACE_OUTER_BOUND ( 'NONE', #21290, .T. ) ;
#20768=LINE ( 'NONE', #2536, #13140 ) ;
#20773=TOROIDAL_SURFACE ( 'NONE', #9601, 4.000000000000000000, 0.2500000000000000000 ) ;
#20797=VERTEX_POINT ( 'NONE', #2967 ) ;
#20801=PLANE ( 'NONE',  #8069 ) ;
#20813=ORIENTED_EDGE ( 'NONE', *, *, #5661, .T. ) ;
#20842=EDGE_CURVE ( 'NONE', #13331, #6133, #8555, .T. ) ;
#20985=CARTESIAN_POINT ( 'NONE',  ( 0.000000000000000000, 1.178949249685218081, 2.041999999999998483 ) ) ;
#20993=AXIS2_PLACEMENT_3D ( 'NONE', #21888, #16253, #5361 ) ;
#21004=VERTEX_POINT ( 'NONE', #13642 ) ;
#21014=EDGE_CURVE ( 'NONE', #12275, #4892, #22515, .T. ) ;
#21016=CARTESIAN_POINT ( 'NONE',  ( 5.000000000000004441, 0.000000000000000000, 4.250000000000000000 ) ) ;
#21027=LINE ( 'NONE', #11896, #6765 ) ;
#21072=CARTESIAN_POINT ( 'NONE',  ( 2.500000000000000000, -1.178949249685213863, 2.042000000000001148 ) ) ;
#21093=DIRECTION ( 'NONE',  ( 0.000000000000000000, 0.5000000000000009992, 0.8660254037844380415 ) ) ;
#21101=VECTOR ( 'NONE', #12224, 1000.000000000000000 ) ;
#21126=EDGE_LOOP ( 'NONE', ( #10401, #1265, #22687, #9045 ) ) ;
#21167=CIRCLE ( 'NONE', #18094, 4.000000000000000000 ) ;
#21202=DIRECTION ( 'NONE',  ( -0.7071067811865254793, 0.000000000000000000, 0.7071067811865695552 ) ) ;
#21215=CIRCLE ( 'NONE', #10834, 0.2000000000000000944 ) ;
#21243=ORIENTED_EDGE ( 'NONE', *, *, #19459, .T. ) ;
#21285=DIRECTION ( 'NONE',  ( 1.000000000000000000, 0.000000000000000000, 0.000000000000000000 ) ) ;
#21290=EDGE_LOOP ( 'NONE', ( #11900, #20813, #18263 ) ) ;
#21318=FILL_AREA_STYLE ('',( #10117 ) ) ;
#21341=DIRECTION ( 'NONE',  ( 0.000000000000000000, -0.4999999999999992228, 0.8660254037844390407 ) ) ;
#21369=ADVANCED_FACE ( 'NONE', ( #13006 ), #22124, .T. ) ;
#21414=VERTEX_POINT ( 'NONE', #12145 ) ;
#21513=VERTEX_POINT ( 'NONE', #19338 ) ;
#21515=VERTEX_POINT ( 'NONE', #2797 ) ;
#21523=CIRCLE ( 'NONE', #22676, 2.041999999999999815 ) ;
#21529=EDGE_CURVE ( 'NONE', #3010, #22378, #6426, .T. ) ;
#21590=CARTESIAN_POINT ( 'NONE',  ( -31.74999999999995737, 0.000000000000000000, 0.000000000000000000 ) ) ;
#21736=ORIENTED_EDGE ( 'NONE', *, *, #6971, .T. ) ;
#21810=DIRECTION ( 'NONE',  ( 0.000000000000000000, 0.000000000000000000, 1.000000000000000000 ) ) ;
#21857=CARTESIAN_POINT ( 'NONE',  ( 2.500000000000000000, 1.178949249685213863, -2.042000000000001148 ) ) ;
#21888=CARTESIAN_POINT ( 'NONE',  ( 34.99999999999999289, 0.000000000000000000, 0.000000000000000000 ) ) ;
#21941=AXIS2_PLACEMENT_3D ( 'NONE', #19029, #2496, #9884 ) ;
#22007=EDGE_CURVE ( 'NONE', #14121, #6031, #12684, .T. ) ;
#22122=AXIS2_PLACEMENT_3D ( 'NONE', #14442, #5245, #1721 ) ;
#22124=PLANE ( 'NONE',  #18468 ) ;
#22128=EDGE_LOOP ( 'NONE', ( #16872, #17980, #15540, #1109, #1573 ) ) ;
#22146=AXIS2_PLACEMENT_3D ( 'NONE', #19082, #855, #180 ) ;
#22150=ORIENTED_EDGE ( 'NONE', *, *, #1046, .T. ) ;
#22180=ORIENTED_EDGE ( 'NONE', *, *, #1733, .T. ) ;
#22218=ORIENTED_EDGE ( 'NONE', *, *, #10602, .T. ) ;
#22230=DIRECTION ( 'NONE',  ( 0.000000000000000000, 0.000000000000000000, 1.000000000000000000 ) ) ;
#22253=VECTOR ( 'NONE', #19463, 1000.000000000000000 ) ;
#22301=CARTESIAN_POINT ( 'NONE',  ( 5.200000000000002842, 0.000000000000000000, 0.000000000000000000 ) ) ;
#22378=VERTEX_POINT ( 'NONE', #3178 ) ;
#22409=( LENGTH_UNIT ( ) NAMED_UNIT ( * ) SI_UNIT ( .MILLI., .METRE. ) );
#22424=DIRECTION ( 'NONE',  ( 0.000000000000000000, -0.4999999999999992228, 0.8660254037844390407 ) ) ;
#22444=DIRECTION ( 'NONE',  ( 1.000000000000000000, 0.000000000000000000, 0.000000000000000000 ) ) ;
#22502=VECTOR ( 'NONE', #14273, 1000.000000000000114 ) ;
#22507=DIRECTION ( 'NONE',  ( 1.000000000000000000, 0.000000000000000000, 0.000000000000000000 ) ) ;
#22513=PLANE ( 'NONE',  #2672 ) ;
#22515=LINE ( 'NONE', #5864, #6498 ) ;
#22604=ORIENTED_EDGE ( 'NONE', *, *, #17747, .T. ) ;
#22606=AXIS2_PLACEMENT_3D ( 'NONE', #10421, #19080, #2545 ) ;
#22643=VECTOR ( 'NONE', #10098, 1000.000000000000114 ) ;
#22676=AXIS2_PLACEMENT_3D ( 'NONE', #11715, #8065, #7816 ) ;
#22687=ORIENTED_EDGE ( 'NONE', *, *, #19584, .T. ) ;
#22829=CYLINDRICAL_SURFACE ( 'NONE', #22146, 2.500000000000000444 ) ;
#22879=SURFACE_STYLE_USAGE ( .BOTH. , #11585 ) ;
#22894=DIRECTION ( 'NONE',  ( 0.000000000000000000, 0.8660254037844380415, -0.5000000000000009992 ) ) ;
#22981=EDGE_LOOP ( 'NONE', ( #18543, #15557 ) ) ;
#22984=DIRECTION ( 'NONE',  ( 0.000000000000000000, 1.000000000000000000, -1.103561164596346103E-15 ) ) ;
#22990=( NAMED_UNIT ( * ) SI_UNIT ( $, .STERADIAN. ) SOLID_ANGLE_UNIT ( ) );
#23012=ORIENTED_EDGE ( 'NONE', *, *, #13501, .F. ) ;
#23061=CARTESIAN_POINT ( 'NONE',  ( 0.000000000000000000, -2.357898499370431722, 2.818925648462311528E-15 ) ) ;
#23085=MECHANICAL_DESIGN_GEOMETRIC_PRESENTATION_REPRESENTATION('',(#1113),#7284);
#23099=AXIS2_PLACEMENT_3D ( 'NONE', #405, #18370, #22230 ) ;
#23114=LINE ( 'NONE', #11938, #10023 ) ;
#23205=EDGE_LOOP ( 'NONE', ( #15762, #15312, #1878, #22150, #15776, #18705 ) ) ;
#23231=CARTESIAN_POINT ( 'NONE',  ( 0.000000000000000000, 2.357898499370432166, -2.385244779468109755E-15 ) ) ;
#23250=PLANE ( 'NONE',  #5798 ) ;
#23313=ADVANCED_FACE ( 'NONE', ( #5274 ), #8794, .T. ) ;
#23341=ORIENTED_EDGE ( 'NONE', *, *, #19584, .F. ) ;
#23354=CARTESIAN_POINT ( 'NONE',  ( 3.678949249685231848, 0.000000000000000000, 0.000000000000000000 ) ) ;
#23450=DIRECTION ( 'NONE',  ( 0.000000000000000000, 0.000000000000000000, 1.000000000000000000 ) ) ;
#23566=DIRECTION ( 'NONE',  ( 0.000000000000000000, -1.000000000000000000, 1.287488025362403787E-15 ) ) ;
#23580=CARTESIAN_POINT ( 'NONE',  ( 2.500000000000000000, -1.178949249685213863, 2.042000000000001148 ) ) ;
#23582=EDGE_CURVE ( 'NONE', #6031, #7824, #9745, .T. ) ;
#23609=DIRECTION ( 'NONE',  ( -1.000000000000000000, -0.000000000000000000, -0.000000000000000000 ) ) ;
#23672=LINE ( 'NONE', #21857, #15748 ) ;
#23921=COLOUR_RGB('Black',0.12,0.14,0.17);
#23922=FILL_AREA_STYLE_COLOUR('',#23921);
#23923=FILL_AREA_STYLE('',(#23922));
#23924=SURFACE_STYLE_FILL_AREA(#23923);
#23925=SURFACE_SIDE_STYLE('',(#23924));
#23926=SURFACE_STYLE_USAGE(.BOTH.,#23925);
#23927=PRESENTATION_STYLE_ASSIGNMENT((#23926));
ENDSEC;
END-ISO-10303-21;
